ISO-10303-21;
HEADER;
FILE_DESCRIPTION (('STEP AP214'),
    '1' );
FILE_NAME ('o-rings series a_iso_O-ring 45x2.65-A-ISO 3601-1.step',
    '2026-10-24T08:20:21',
    ( '' ),
    ( '' ),
    'SwSTEP 2.0',
    'SolidWorks 2026',
    '' );
FILE_SCHEMA (( 'AUTOMOTIVE_DESIGN' ));
ENDSEC;

DATA;
#61=DIRECTION ( 'NONE',  ( -1.000000000000000000, -1.224646799147352961E-16, 0.000000000000000000 ) ) ;
#62=AXIS2_PLACEMENT_3D ( 'NONE', #1095, #2604, #3467 ) ;
#83=AXIS2_PLACEMENT_3D ( 'NONE', #3751, #2911, #1411 ) ;
#106=EDGE_CURVE ( 'NONE', #1824, #3785, #3518, .T. ) ;
#211=TOROIDAL_SURFACE ( 'NONE', #83, 23.82500000000000284, 1.324999999999999956 ) ;
#258=AXIS2_PLACEMENT_3D ( 'NONE', #2656, #623, #2632 ) ;
#320=CARTESIAN_POINT ( 'NONE',  ( 0.000000000000000000, 0.000000000000000000, 1.622657008870242981E-16 ) ) ;
#322=SURFACE_SIDE_STYLE ('',( #3002 ) ) ;
#342=UNCERTAINTY_MEASURE_WITH_UNIT (LENGTH_MEASURE( 1.000000000000000082E-05 ), #3816, 'distance_accuracy_value', 'NONE');
#358=CLOSED_SHELL ( 'NONE', ( #3036, #435, #1819, #2343 ) ) ;
#368=EDGE_CURVE ( 'NONE', #1824, #1740, #3586, .T. ) ;
#396=( GEOMETRIC_REPRESENTATION_CONTEXT ( 3 ) GLOBAL_UNCERTAINTY_ASSIGNED_CONTEXT ( ( #342 ) ) GLOBAL_UNIT_ASSIGNED_CONTEXT ( ( #3816, #2730, #3306 ) ) REPRESENTATION_CONTEXT ( 'NONE', 'WORKASPACE' ) );
#424=ORIENTED_EDGE ( 'NONE', *, *, #368, .T. ) ;
#429=FACE_OUTER_BOUND ( 'NONE', #2125, .T. ) ;
#435=ADVANCED_FACE ( 'NONE', ( #429 ), #976, .T. ) ;
#478=FACE_OUTER_BOUND ( 'NONE', #890, .T. ) ;
#480=DIRECTION ( 'NONE',  ( 0.000000000000000000, -1.000000000000000000, 0.000000000000000000 ) ) ;
#496=CARTESIAN_POINT ( 'NONE',  ( 0.000000000000000000, 0.000000000000000000, 0.000000000000000000 ) ) ;
#589=EDGE_CURVE ( 'NONE', #3785, #3235, #2707, .T. ) ;
#623=DIRECTION ( 'NONE',  ( -0.000000000000000000, -0.000000000000000000, -1.000000000000000000 ) ) ;
#649=ORIENTED_EDGE ( 'NONE', *, *, #2423, .F. ) ;
#729=CARTESIAN_POINT ( 'NONE',  ( 23.82500000000000284, 2.917720998968569322E-15, 0.000000000000000000 ) ) ;
#774=CARTESIAN_POINT ( 'NONE',  ( -23.82500000000000284, 0.000000000000000000, 0.000000000000000000 ) ) ;
#782=AXIS2_PLACEMENT_3D ( 'NONE', #1045, #3410, #1636 ) ;
#793=ORIENTED_EDGE ( 'NONE', *, *, #1047, .F. ) ;
#820=CARTESIAN_POINT ( 'NONE',  ( 0.000000000000000000, 0.000000000000000000, 0.000000000000000000 ) ) ;
#823=( LENGTH_UNIT ( ) NAMED_UNIT ( * ) SI_UNIT ( .MILLI., .METRE. ) );
#846=CIRCLE ( 'NONE', #782, 1.324999999999999734 ) ;
#886=ORIENTED_EDGE ( 'NONE', *, *, #3729, .T. ) ;
#890=EDGE_LOOP ( 'NONE', ( #3130, #1702, #3800, #649 ) ) ;
#923=CARTESIAN_POINT ( 'NONE',  ( 25.15000000000000213, 3.079986699855593473E-15, 0.000000000000000000 ) ) ;
#947=CARTESIAN_POINT ( 'NONE',  ( 0.000000000000000000, 0.000000000000000000, 1.622657008870242981E-16 ) ) ;
#948=TOROIDAL_SURFACE ( 'NONE', #2565, 23.82500000000000284, 1.324999999999999956 ) ;
#976=TOROIDAL_SURFACE ( 'NONE', #2291, 23.82500000000000284, 1.324999999999999956 ) ;
#1045=CARTESIAN_POINT ( 'NONE',  ( 23.82500000000000284, 2.917720998968569322E-15, 0.000000000000000000 ) ) ;
#1046=PRODUCT ( 'o-rings series a_iso_O-ring 45x2.65-A-ISO 3601-1', 'o-rings series a_iso_O-ring 45x2.65-A-ISO 3601-1', '', ( #3427 ) ) ;
#1047=EDGE_CURVE ( 'NONE', #3785, #1824, #3150, .T. ) ;
#1095=CARTESIAN_POINT ( 'NONE',  ( -23.82500000000000284, 0.000000000000000000, 0.000000000000000000 ) ) ;
#1110=DIRECTION ( 'NONE',  ( 0.000000000000000000, 0.000000000000000000, -1.000000000000000000 ) ) ;
#1132=SURFACE_STYLE_USAGE ( .BOTH. , #322 ) ;
#1162=EDGE_LOOP ( 'NONE', ( #2023, #793, #1218, #1178 ) ) ;
#1178=ORIENTED_EDGE ( 'NONE', *, *, #3801, .T. ) ;
#1218=ORIENTED_EDGE ( 'NONE', *, *, #589, .T. ) ;
#1226=DIRECTION ( 'NONE',  ( -1.000000000000000000, 0.000000000000000000, 0.000000000000000000 ) ) ;
#1265=CIRCLE ( 'NONE', #3441, 22.50000000000000355 ) ;
#1367=( NAMED_UNIT ( * ) SI_UNIT ( $, .STERADIAN. ) SOLID_ANGLE_UNIT ( ) );
#1411=DIRECTION ( 'NONE',  ( -1.000000000000000000, 0.000000000000000000, 0.000000000000000000 ) ) ;
#1454=ORIENTED_EDGE ( 'NONE', *, *, #3508, .F. ) ;
#1513=AXIS2_PLACEMENT_3D ( 'NONE', #320, #3560, #3601 ) ;
#1517=CIRCLE ( 'NONE', #3636, 1.324999999999999734 ) ;
#1521=EDGE_LOOP ( 'NONE', ( #1454, #2845, #2307, #2636 ) ) ;
#1632=AXIS2_PLACEMENT_3D ( 'NONE', #496, #1689, #2869 ) ;
#1636=DIRECTION ( 'NONE',  ( -1.000000000000000000, -1.224646799147352961E-16, 0.000000000000000000 ) ) ;
#1647=COLOUR_RGB ( '',1.000000000000000000, 0.9490196078431372140, 0.9098039215686274384 ) ;
#1689=DIRECTION ( 'NONE',  ( -0.000000000000000000, -0.000000000000000000, -1.000000000000000000 ) ) ;
#1702=ORIENTED_EDGE ( 'NONE', *, *, #3508, .T. ) ;
#1703=( NAMED_UNIT ( * ) PLANE_ANGLE_UNIT ( ) SI_UNIT ( $, .RADIAN. ) );
#1740=VERTEX_POINT ( 'NONE', #923 ) ;
#1751=SHAPE_REPRESENTATION ( 'o-rings series a_iso_O-ring 45x2.65-A-ISO 3601-1', ( #2207 ), #3327 ) ;
#1810=( NAMED_UNIT ( * ) SI_UNIT ( $, .STERADIAN. ) SOLID_ANGLE_UNIT ( ) );
#1818=STYLED_ITEM('',(#3881),#3290);
#1819=ADVANCED_FACE ( 'NONE', ( #2288 ), #948, .T. ) ;
#1824=VERTEX_POINT ( 'NONE', #3104 ) ;
#1832=SHAPE_REPRESENTATION_RELATIONSHIP ( 'NONE' , 'NONE' ,  #1751, #2924 ) ;
#1835=DIRECTION ( 'NONE',  ( -1.224646799147353207E-16, 1.000000000000000000, 0.000000000000000000 ) ) ;
#1901=ORIENTED_EDGE ( 'NONE', *, *, #106, .F. ) ;
#1975=PRODUCT_DEFINITION_SHAPE ( 'NONE', 'NONE',  #3576 ) ;
#2023=ORIENTED_EDGE ( 'NONE', *, *, #368, .F. ) ;
#2083=AXIS2_PLACEMENT_3D ( 'NONE', #2371, #3832, #1226 ) ;
#2125=EDGE_LOOP ( 'NONE', ( #1901, #424, #886, #3032 ) ) ;
#2128=DIRECTION ( 'NONE',  ( -0.000000000000000000, -0.000000000000000000, -1.000000000000000000 ) ) ;
#2207=AXIS2_PLACEMENT_3D ( 'NONE', #820, #2246, #3194 ) ;
#2246=DIRECTION ( 'NONE',  ( 0.000000000000000000, 0.000000000000000000, 1.000000000000000000 ) ) ;
#2288=FACE_OUTER_BOUND ( 'NONE', #1162, .T. ) ;
#2291=AXIS2_PLACEMENT_3D ( 'NONE', #3420, #2760, #2445 ) ;
#2294=CARTESIAN_POINT ( 'NONE',  ( -22.50000000000000355, 0.000000000000000000, 1.622657008870243228E-16 ) ) ;
#2307=ORIENTED_EDGE ( 'NONE', *, *, #2423, .T. ) ;
#2325=TOROIDAL_SURFACE ( 'NONE', #1632, 23.82500000000000284, 1.324999999999999956 ) ;
#2343=ADVANCED_FACE ( 'NONE', ( #2914 ), #2325, .T. ) ;
#2371=CARTESIAN_POINT ( 'NONE',  ( 0.000000000000000000, 0.000000000000000000, 0.000000000000000000 ) ) ;
#2423=EDGE_CURVE ( 'NONE', #3235, #3785, #1265, .T. ) ;
#2445=DIRECTION ( 'NONE',  ( -1.000000000000000000, 0.000000000000000000, 0.000000000000000000 ) ) ;
#2488=APPLICATION_CONTEXT ( 'automotive_design' ) ;
#2525=AXIS2_PLACEMENT_3D ( 'NONE', #774, #480, #1110 ) ;
#2531=PRODUCT_DEFINITION_FORMATION_WITH_SPECIFIED_SOURCE ( 'ANY', '', #1046, .NOT_KNOWN. ) ;
#2553=SHAPE_DEFINITION_REPRESENTATION ( #1975, #1751 ) ;
#2565=AXIS2_PLACEMENT_3D ( 'NONE', #2798, #3447, #3468 ) ;
#2578=UNCERTAINTY_MEASURE_WITH_UNIT (LENGTH_MEASURE( 1.000000000000000082E-05 ), #2716, 'distance_accuracy_value', 'NONE');
#2604=DIRECTION ( 'NONE',  ( 0.000000000000000000, -1.000000000000000000, 0.000000000000000000 ) ) ;
#2632=DIRECTION ( 'NONE',  ( -1.000000000000000000, 0.000000000000000000, 0.000000000000000000 ) ) ;
#2636=ORIENTED_EDGE ( 'NONE', *, *, #1047, .T. ) ;
#2643=MECHANICAL_DESIGN_GEOMETRIC_PRESENTATION_REPRESENTATION('',(#3820),#396);
#2656=CARTESIAN_POINT ( 'NONE',  ( 0.000000000000000000, 0.000000000000000000, 0.000000000000000000 ) ) ;
#2690=FILL_AREA_STYLE_COLOUR ( '', #1647 ) ;
#2707=CIRCLE ( 'NONE', #1513, 22.50000000000000355 ) ;
#2716=( LENGTH_UNIT ( ) NAMED_UNIT ( * ) SI_UNIT ( .MILLI., .METRE. ) );
#2730=( NAMED_UNIT ( * ) PLANE_ANGLE_UNIT ( ) SI_UNIT ( $, .RADIAN. ) );
#2760=DIRECTION ( 'NONE',  ( -0.000000000000000000, -0.000000000000000000, -1.000000000000000000 ) ) ;
#2798=CARTESIAN_POINT ( 'NONE',  ( 0.000000000000000000, 0.000000000000000000, 0.000000000000000000 ) ) ;
#2845=ORIENTED_EDGE ( 'NONE', *, *, #3801, .F. ) ;
#2869=DIRECTION ( 'NONE',  ( -1.000000000000000000, 0.000000000000000000, 0.000000000000000000 ) ) ;
#2879=MECHANICAL_DESIGN_GEOMETRIC_PRESENTATION_REPRESENTATION('',(#1818),#3376);
#2890=PRODUCT_DEFINITION_CONTEXT ( 'detailed design', #3415, 'design' ) ;
#2911=DIRECTION ( 'NONE',  ( -0.000000000000000000, -0.000000000000000000, -1.000000000000000000 ) ) ;
#2914=FACE_OUTER_BOUND ( 'NONE', #1521, .T. ) ;
#2924=ADVANCED_BREP_SHAPE_REPRESENTATION ( '', ( #3290, #2207 ), #3327 ) ;
#2985=( NAMED_UNIT ( * ) PLANE_ANGLE_UNIT ( ) SI_UNIT ( $, .RADIAN. ) );
#3002=SURFACE_STYLE_FILL_AREA ( #3588 ) ;
#3010=CARTESIAN_POINT ( 'NONE',  ( 22.50000000000000355, 2.755455298081545172E-15, 0.000000000000000000 ) ) ;
#3032=ORIENTED_EDGE ( 'NONE', *, *, #589, .F. ) ;
#3036=ADVANCED_FACE ( 'NONE', ( #478 ), #211, .T. ) ;
#3104=CARTESIAN_POINT ( 'NONE',  ( -25.15000000000000213, 0.000000000000000000, 0.000000000000000000 ) ) ;
#3130=ORIENTED_EDGE ( 'NONE', *, *, #3729, .F. ) ;
#3150=CIRCLE ( 'NONE', #2525, 1.324999999999999956 ) ;
#3194=DIRECTION ( 'NONE',  ( 1.000000000000000000, 0.000000000000000000, 0.000000000000000000 ) ) ;
#3235=VERTEX_POINT ( 'NONE', #3010 ) ;
#3290=MANIFOLD_SOLID_BREP ( 'Sweep1', #358 ) ;
#3306=( NAMED_UNIT ( * ) SI_UNIT ( $, .STERADIAN. ) SOLID_ANGLE_UNIT ( ) );
#3327=( GEOMETRIC_REPRESENTATION_CONTEXT ( 3 ) GLOBAL_UNCERTAINTY_ASSIGNED_CONTEXT ( ( #2578 ) ) GLOBAL_UNIT_ASSIGNED_CONTEXT ( ( #2716, #2985, #1810 ) ) REPRESENTATION_CONTEXT ( 'NONE', 'WORKASPACE' ) );
#3376=( GEOMETRIC_REPRESENTATION_CONTEXT ( 3 ) GLOBAL_UNCERTAINTY_ASSIGNED_CONTEXT ( ( #3711 ) ) GLOBAL_UNIT_ASSIGNED_CONTEXT ( ( #823, #1703, #1367 ) ) REPRESENTATION_CONTEXT ( 'NONE', 'WORKASPACE' ) );
#3410=DIRECTION ( 'NONE',  ( -1.224646799147353207E-16, 1.000000000000000000, 0.000000000000000000 ) ) ;
#3415=APPLICATION_CONTEXT ( 'automotive_design' ) ;
#3420=CARTESIAN_POINT ( 'NONE',  ( 0.000000000000000000, 0.000000000000000000, 0.000000000000000000 ) ) ;
#3427=PRODUCT_CONTEXT ( 'NONE', #2488, 'mechanical' ) ;
#3441=AXIS2_PLACEMENT_3D ( 'NONE', #947, #2128, #3631 ) ;
#3447=DIRECTION ( 'NONE',  ( -0.000000000000000000, -0.000000000000000000, -1.000000000000000000 ) ) ;
#3467=DIRECTION ( 'NONE',  ( 0.000000000000000000, 0.000000000000000000, -1.000000000000000000 ) ) ;
#3468=DIRECTION ( 'NONE',  ( -1.000000000000000000, 0.000000000000000000, 0.000000000000000000 ) ) ;
#3505=PRESENTATION_STYLE_ASSIGNMENT (( #1132 ) ) ;
#3508=EDGE_CURVE ( 'NONE', #1740, #1824, #3807, .T. ) ;
#3518=CIRCLE ( 'NONE', #62, 1.324999999999999956 ) ;
#3560=DIRECTION ( 'NONE',  ( -0.000000000000000000, -0.000000000000000000, -1.000000000000000000 ) ) ;
#3576=PRODUCT_DEFINITION ( 'UNKNOWN', '', #2531, #2890 ) ;
#3586=CIRCLE ( 'NONE', #2083, 25.15000000000000213 ) ;
#3588=FILL_AREA_STYLE ('',( #2690 ) ) ;
#3601=DIRECTION ( 'NONE',  ( -1.000000000000000000, 0.000000000000000000, 0.000000000000000000 ) ) ;
#3631=DIRECTION ( 'NONE',  ( -1.000000000000000000, 0.000000000000000000, 0.000000000000000000 ) ) ;
#3636=AXIS2_PLACEMENT_3D ( 'NONE', #729, #1835, #61 ) ;
#3711=UNCERTAINTY_MEASURE_WITH_UNIT (LENGTH_MEASURE( 1.000000000000000082E-05 ), #823, 'distance_accuracy_value', 'NONE');
#3729=EDGE_CURVE ( 'NONE', #1740, #3235, #1517, .T. ) ;
#3751=CARTESIAN_POINT ( 'NONE',  ( 0.000000000000000000, 0.000000000000000000, 0.000000000000000000 ) ) ;
#3785=VERTEX_POINT ( 'NONE', #2294 ) ;
#3800=ORIENTED_EDGE ( 'NONE', *, *, #106, .T. ) ;
#3801=EDGE_CURVE ( 'NONE', #3235, #1740, #846, .T. ) ;
#3807=CIRCLE ( 'NONE', #258, 25.15000000000000213 ) ;
#3816=( LENGTH_UNIT ( ) NAMED_UNIT ( * ) SI_UNIT ( .MILLI., .METRE. ) );
#3820=STYLED_ITEM ( 'NONE', ( #3505 ), #2924 ) ;
#3832=DIRECTION ( 'NONE',  ( -0.000000000000000000, -0.000000000000000000, -1.000000000000000000 ) ) ;
#3875=COLOUR_RGB('Black',0.12,0.14,0.17);
#3876=FILL_AREA_STYLE_COLOUR('',#3875);
#3877=FILL_AREA_STYLE('',(#3876));
#3878=SURFACE_STYLE_FILL_AREA(#3877);
#3879=SURFACE_SIDE_STYLE('',(#3878));
#3880=SURFACE_STYLE_USAGE(.BOTH.,#3879);
#3881=PRESENTATION_STYLE_ASSIGNMENT((#3880));
ENDSEC;
END-ISO-10303-21;
